ISO-10303-21;
HEADER;
FILE_DESCRIPTION (('STEP AP214'),
    '1' );
FILE_NAME ('Bolt2.step',
    '2026-10-28T16:39:03',
    ( '' ),
    ( '' ),
    'SwSTEP 2.0',
    'SolidWorks 2024',
    '' );
FILE_SCHEMA (( 'AUTOMOTIVE_DESIGN' ));
ENDSEC;

DATA;
#38=CARTESIAN_POINT ( 'NONE',  ( 0.000000000000000000, 0.000000000000000000, 75.00000000000000000 ) ) ;
#48=FACE_OUTER_BOUND ( 'NONE', #2158, .T. ) ;
#93=EDGE_LOOP ( 'NONE', ( #2797, #6100, #4748, #419 ) ) ;
#116=VERTEX_POINT ( 'NONE', #2354 ) ;
#179=AXIS2_PLACEMENT_3D ( 'NONE', #6550, #500, #1729 ) ;
#180=AXIS2_PLACEMENT_3D ( 'NONE', #6279, #3725, #665 ) ;
#222=AXIS2_PLACEMENT_3D ( 'NONE', #38, #3852, #5502 ) ;
#231=EDGE_CURVE ( 'NONE', #6488, #3881, #4145, .T. ) ;
#275=PRODUCT_DEFINITION_SHAPE ( 'NONE', 'NONE',  #6885 ) ;
#305=CARTESIAN_POINT ( 'NONE',  ( 17.50000000000000355, 2.143131898507868643E-15, 82.49999999999998579 ) ) ;
#328=CIRCLE ( 'NONE', #4299, 12.50000000000000000 ) ;
#341=SHAPE_REPRESENTATION ( 'Bolt2', ( #5785 ), #4108 ) ;
#351=DIRECTION ( 'NONE',  ( -0.000000000000000000, -0.000000000000000000, -1.000000000000000000 ) ) ;
#366=AXIS2_PLACEMENT_3D ( 'NONE', #6709, #5470, #691 ) ;
#395=EDGE_CURVE ( 'NONE', #2843, #1677, #2239, .T. ) ;
#419=ORIENTED_EDGE ( 'NONE', *, *, #1254, .F. ) ;
#469=ORIENTED_EDGE ( 'NONE', *, *, #2265, .T. ) ;
#473=EDGE_CURVE ( 'NONE', #116, #3864, #3982, .T. ) ;
#500=DIRECTION ( 'NONE',  ( -0.000000000000000000, -0.000000000000000000, -1.000000000000000000 ) ) ;
#506=AXIS2_PLACEMENT_3D ( 'NONE', #6371, #2247, #3882 ) ;
#589=EDGE_LOOP ( 'NONE', ( #4960, #6697, #7720, #5853 ) ) ;
#590=( LENGTH_UNIT ( ) NAMED_UNIT ( * ) SI_UNIT ( .MILLI., .METRE. ) );
#628=CIRCLE ( 'NONE', #3315, 12.50000000000000355 ) ;
#633=ADVANCED_FACE ( 'NONE', ( #48 ), #1218, .T. ) ;
#665=DIRECTION ( 'NONE',  ( 1.000000000000000000, 0.000000000000000000, 0.000000000000000000 ) ) ;
#691=DIRECTION ( 'NONE',  ( 1.000000000000000000, 0.000000000000000000, 0.000000000000000000 ) ) ;
#749=EDGE_LOOP ( 'NONE', ( #6564, #6414, #6580, #3207 ) ) ;
#753=CARTESIAN_POINT ( 'NONE',  ( -12.50000000000000000, 0.000000000000000000, 75.00000000000000000 ) ) ;
#783=UNCERTAINTY_MEASURE_WITH_UNIT (LENGTH_MEASURE( 1.000000000000000082E-05 ), #590, 'distance_accuracy_value', 'NONE');
#793=CARTESIAN_POINT ( 'NONE',  ( 0.000000000000000000, 0.000000000000000000, 2.000000000000001776 ) ) ;
#814=SHAPE_REPRESENTATION_RELATIONSHIP ( 'NONE' , 'NONE' ,  #341, #3928 ) ;
#832=FACE_OUTER_BOUND ( 'NONE', #4118, .T. ) ;
#833=VECTOR ( 'NONE', #6443, 1000.000000000000000 ) ;
#844=DIRECTION ( 'NONE',  ( -0.000000000000000000, -0.000000000000000000, -1.000000000000000000 ) ) ;
#858=DIRECTION ( 'NONE',  ( 1.000000000000000000, 0.000000000000000000, 0.000000000000000000 ) ) ;
#910=LINE ( 'NONE', #1586, #5309 ) ;
#931=EDGE_LOOP ( 'NONE', ( #3127, #1836, #5610, #1028 ) ) ;
#1000=CARTESIAN_POINT ( 'NONE',  ( 0.000000000000000000, 0.000000000000000000, 75.00000000000000000 ) ) ;
#1002=DIRECTION ( 'NONE',  ( -0.000000000000000000, -0.000000000000000000, -1.000000000000000000 ) ) ;
#1004=AXIS2_PLACEMENT_3D ( 'NONE', #1000, #5856, #4787 ) ;
#1016=CIRCLE ( 'NONE', #3076, 5.000000000000004441 ) ;
#1028=ORIENTED_EDGE ( 'NONE', *, *, #5917, .F. ) ;
#1035=DIRECTION ( 'NONE',  ( -1.000000000000000000, 0.000000000000000000, 0.000000000000000000 ) ) ;
#1108=VERTEX_POINT ( 'NONE', #7792 ) ;
#1135=CIRCLE ( 'NONE', #506, 10.49999999999999467 ) ;
#1152=ORIENTED_EDGE ( 'NONE', *, *, #473, .F. ) ;
#1180=CARTESIAN_POINT ( 'NONE',  ( 0.000000000000000000, 0.000000000000000000, 75.00000000000000000 ) ) ;
#1212=AXIS2_PLACEMENT_3D ( 'NONE', #3350, #7122, #5800 ) ;
#1217=DIRECTION ( 'NONE',  ( 0.000000000000000000, 0.000000000000000000, 1.000000000000000000 ) ) ;
#1218=PLANE ( 'NONE',  #7750 ) ;
#1254=EDGE_CURVE ( 'NONE', #1108, #3864, #3024, .T. ) ;
#1269=DIRECTION ( 'NONE',  ( 0.000000000000000000, 0.000000000000000000, 1.000000000000000000 ) ) ;
#1291=CARTESIAN_POINT ( 'NONE',  ( -17.50000000000000355, 0.000000000000000000, 77.49999999999998579 ) ) ;
#1301=( NAMED_UNIT ( * ) PLANE_ANGLE_UNIT ( ) SI_UNIT ( $, .RADIAN. ) );
#1351=ORIENTED_EDGE ( 'NONE', *, *, #395, .F. ) ;
#1383=MANIFOLD_SOLID_BREP ( 'Pah2', #6579 ) ;
#1419=CARTESIAN_POINT ( 'NONE',  ( 0.000000000000000000, 0.000000000000000000, 75.00000000000000000 ) ) ;
#1448=EDGE_CURVE ( 'NONE', #2355, #1785, #7368, .T. ) ;
#1486=DIRECTION ( 'NONE',  ( -0.000000000000000000, -0.000000000000000000, 1.000000000000000000 ) ) ;
#1500=CARTESIAN_POINT ( 'NONE',  ( 12.50000000000000000, 1.530808498934191521E-15, 75.00000000000000000 ) ) ;
#1586=CARTESIAN_POINT ( 'NONE',  ( -12.50000000000000000, 0.000000000000000000, 75.00000000000000000 ) ) ;
#1622=ADVANCED_FACE ( 'NONE', ( #3198 ), #5959, .T. ) ;
#1629=CIRCLE ( 'NONE', #222, 12.50000000000000000 ) ;
#1647=AXIS2_PLACEMENT_3D ( 'NONE', #5772, #5115, #2598 ) ;
#1667=ORIENTED_EDGE ( 'NONE', *, *, #6328, .F. ) ;
#1677=VERTEX_POINT ( 'NONE', #7635 ) ;
#1729=DIRECTION ( 'NONE',  ( 1.000000000000000000, 0.000000000000000000, 0.000000000000000000 ) ) ;
#1734=ADVANCED_FACE ( 'NONE', ( #3511 ), #4105, .T. ) ;
#1785=VERTEX_POINT ( 'NONE', #6636 ) ;
#1831=EDGE_CURVE ( 'NONE', #116, #6898, #4011, .T. ) ;
#1836=ORIENTED_EDGE ( 'NONE', *, *, #7458, .F. ) ;
#1914=DIRECTION ( 'NONE',  ( -1.000000000000000000, 1.224646799147353454E-16, 0.000000000000000000 ) ) ;
#1941=CARTESIAN_POINT ( 'NONE',  ( 0.000000000000000000, 0.000000000000000000, 77.49999999999998579 ) ) ;
#1989=DIRECTION ( 'NONE',  ( 1.224646799147353207E-16, 1.000000000000000000, -0.000000000000000000 ) ) ;
#2003=CARTESIAN_POINT ( 'NONE',  ( 12.50000000000000355, 0.000000000000000000, 82.49999999999998579 ) ) ;
#2094=AXIS2_PLACEMENT_3D ( 'NONE', #1419, #3870, #858 ) ;
#2158=EDGE_LOOP ( 'NONE', ( #3332, #7881 ) ) ;
#2164=ORIENTED_EDGE ( 'NONE', *, *, #1448, .F. ) ;
#2227=CIRCLE ( 'NONE', #179, 17.50000000000000355 ) ;
#2239=CIRCLE ( 'NONE', #2094, 17.50000000000000355 ) ;
#2247=DIRECTION ( 'NONE',  ( -0.000000000000000000, -0.000000000000000000, -1.000000000000000000 ) ) ;
#2265=EDGE_CURVE ( 'NONE', #1785, #2355, #2227, .T. ) ;
#2315=DIRECTION ( 'NONE',  ( 1.000000000000000000, 0.000000000000000000, 0.000000000000000000 ) ) ;
#2319=ORIENTED_EDGE ( 'NONE', *, *, #2984, .F. ) ;
#2336=PLANE ( 'NONE',  #4849 ) ;
#2351=DIRECTION ( 'NONE',  ( 1.000000000000000000, 0.000000000000000000, 0.000000000000000000 ) ) ;
#2354=CARTESIAN_POINT ( 'NONE',  ( 12.50000000000000000, 1.530808498934191521E-15, 75.00000000000000000 ) ) ;
#2355=VERTEX_POINT ( 'NONE', #1291 ) ;
#2467=ORIENTED_EDGE ( 'NONE', *, *, #4772, .T. ) ;
#2530=CARTESIAN_POINT ( 'NONE',  ( 12.50000000000000355, 0.000000000000000000, 77.49999999999998579 ) ) ;
#2540=DIRECTION ( 'NONE',  ( 0.000000000000000000, 0.000000000000000000, 1.000000000000000000 ) ) ;
#2581=EDGE_CURVE ( 'NONE', #2355, #2843, #6378, .T. ) ;
#2598=DIRECTION ( 'NONE',  ( 1.000000000000000000, 0.000000000000000000, 0.000000000000000000 ) ) ;
#2732=VECTOR ( 'NONE', #4855, 999.9999999999998863 ) ;
#2736=DIRECTION ( 'NONE',  ( 1.000000000000000000, 0.000000000000000000, 0.000000000000000000 ) ) ;
#2797=ORIENTED_EDGE ( 'NONE', *, *, #4772, .F. ) ;
#2843=VERTEX_POINT ( 'NONE', #7421 ) ;
#2861=DIRECTION ( 'NONE',  ( -0.000000000000000000, -0.000000000000000000, -1.000000000000000000 ) ) ;
#2929=ORIENTED_EDGE ( 'NONE', *, *, #5293, .F. ) ;
#2937=EDGE_CURVE ( 'NONE', #4729, #6728, #4319, .T. ) ;
#2959=EDGE_CURVE ( 'NONE', #1785, #1677, #6368, .T. ) ;
#2984=EDGE_CURVE ( 'NONE', #6898, #6728, #910, .T. ) ;
#3004=DIRECTION ( 'NONE',  ( -0.000000000000000000, -0.000000000000000000, -1.000000000000000000 ) ) ;
#3008=VECTOR ( 'NONE', #6433, 1000.000000000000000 ) ;
#3024=LINE ( 'NONE', #7312, #2732 ) ;
#3029=ADVANCED_FACE ( 'NONE', ( #832 ), #3401, .T. ) ;
#3030=CARTESIAN_POINT ( 'NONE',  ( 0.000000000000000000, 0.000000000000000000, 82.49999999999998579 ) ) ;
#3076=AXIS2_PLACEMENT_3D ( 'NONE', #2530, #4889, #5585 ) ;
#3078=DIRECTION ( 'NONE',  ( 0.000000000000000000, 0.000000000000000000, 1.000000000000000000 ) ) ;
#3082=ORIENTED_EDGE ( 'NONE', *, *, #4883, .F. ) ;
#3085=CARTESIAN_POINT ( 'NONE',  ( 0.000000000000000000, 0.000000000000000000, 0.000000000000000000 ) ) ;
#3106=PRODUCT_DEFINITION_FORMATION_WITH_SPECIFIED_SOURCE ( 'ANY', '', #3417, .NOT_KNOWN. ) ;
#3117=DIRECTION ( 'NONE',  ( 1.000000000000000000, 0.000000000000000000, -0.000000000000000000 ) ) ;
#3127=ORIENTED_EDGE ( 'NONE', *, *, #2937, .F. ) ;
#3169=FACE_OUTER_BOUND ( 'NONE', #589, .T. ) ;
#3170=DIRECTION ( 'NONE',  ( -0.7071067811865482389, 8.659560562354941486E-17, 0.7071067811865469066 ) ) ;
#3198=FACE_OUTER_BOUND ( 'NONE', #3638, .T. ) ;
#3207=ORIENTED_EDGE ( 'NONE', *, *, #2581, .F. ) ;
#3211=ADVANCED_FACE ( 'NONE', ( #3522 ), #4117, .T. ) ;
#3282=CARTESIAN_POINT ( 'NONE',  ( 0.000000000000000000, 0.000000000000000000, 75.00000000000000000 ) ) ;
#3312=DIRECTION ( 'NONE',  ( 0.000000000000000000, 0.000000000000000000, 1.000000000000000000 ) ) ;
#3315=AXIS2_PLACEMENT_3D ( 'NONE', #6230, #1217, #5634 ) ;
#3332=ORIENTED_EDGE ( 'NONE', *, *, #231, .T. ) ;
#3350=CARTESIAN_POINT ( 'NONE',  ( 0.000000000000000000, 0.000000000000000000, 75.00000000000000000 ) ) ;
#3401=CYLINDRICAL_SURFACE ( 'NONE', #7366, 12.50000000000000000 ) ;
#3417=PRODUCT ( 'Bolt2', 'Bolt2', '', ( #5951 ) ) ;
#3457=DIRECTION ( 'NONE',  ( 1.000000000000000000, 0.000000000000000000, 0.000000000000000000 ) ) ;
#3511=FACE_OUTER_BOUND ( 'NONE', #7877, .T. ) ;
#3522=FACE_OUTER_BOUND ( 'NONE', #749, .T. ) ;
#3565=EDGE_CURVE ( 'NONE', #3864, #6728, #328, .T. ) ;
#3618=CARTESIAN_POINT ( 'NONE',  ( 0.000000000000000000, 0.000000000000000000, 0.000000000000000000 ) ) ;
#3638=EDGE_LOOP ( 'NONE', ( #2164, #4874, #4741, #1667 ) ) ;
#3651=AXIS2_PLACEMENT_3D ( 'NONE', #1941, #3312, #4381 ) ;
#3661=DIRECTION ( 'NONE',  ( 0.000000000000000000, 0.000000000000000000, 1.000000000000000000 ) ) ;
#3672=CIRCLE ( 'NONE', #4681, 5.000000000000000888 ) ;
#3725=DIRECTION ( 'NONE',  ( 0.000000000000000000, 0.000000000000000000, 1.000000000000000000 ) ) ;
#3760=EDGE_CURVE ( 'NONE', #2355, #3881, #3672, .T. ) ;
#3792=ORIENTED_EDGE ( 'NONE', *, *, #3565, .T. ) ;
#3808=CIRCLE ( 'NONE', #6241, 10.49999999999999467 ) ;
#3841=CARTESIAN_POINT ( 'NONE',  ( 12.50000000000000000, 1.530808498934191521E-15, 2.000000000000001776 ) ) ;
#3852=DIRECTION ( 'NONE',  ( 0.000000000000000000, 0.000000000000000000, 1.000000000000000000 ) ) ;
#3864=VERTEX_POINT ( 'NONE', #3841 ) ;
#3870=DIRECTION ( 'NONE',  ( 0.000000000000000000, 0.000000000000000000, 1.000000000000000000 ) ) ;
#3881=VERTEX_POINT ( 'NONE', #5113 ) ;
#3882=DIRECTION ( 'NONE',  ( 1.000000000000000000, 0.000000000000000000, 0.000000000000000000 ) ) ;
#3902=ORIENTED_EDGE ( 'NONE', *, *, #1831, .F. ) ;
#3928=ADVANCED_BREP_SHAPE_REPRESENTATION ( '', ( #1383, #5785 ), #4108 ) ;
#3953=AXIS2_PLACEMENT_3D ( 'NONE', #3030, #4480, #6034 ) ;
#3982=LINE ( 'NONE', #1500, #3008 ) ;
#3985=PRODUCT_DEFINITION_CONTEXT ( 'detailed design', #7820, 'design' ) ;
#4011=CIRCLE ( 'NONE', #5574, 12.50000000000000000 ) ;
#4105=CYLINDRICAL_SURFACE ( 'NONE', #1212, 12.50000000000000000 ) ;
#4108=( GEOMETRIC_REPRESENTATION_CONTEXT ( 3 ) GLOBAL_UNCERTAINTY_ASSIGNED_CONTEXT ( ( #783 ) ) GLOBAL_UNIT_ASSIGNED_CONTEXT ( ( #590, #1301, #5477 ) ) REPRESENTATION_CONTEXT ( 'NONE', 'WORKASPACE' ) );
#4110=CARTESIAN_POINT ( 'NONE',  ( 0.000000000000000000, 0.000000000000000000, 0.000000000000000000 ) ) ;
#4117=CYLINDRICAL_SURFACE ( 'NONE', #4675, 17.50000000000000355 ) ;
#4118=EDGE_LOOP ( 'NONE', ( #3902, #6955, #3792, #2319 ) ) ;
#4145=CIRCLE ( 'NONE', #180, 12.50000000000000355 ) ;
#4186=DIRECTION ( 'NONE',  ( 0.000000000000000000, 0.000000000000000000, 1.000000000000000000 ) ) ;
#4226=ORIENTED_EDGE ( 'NONE', *, *, #2581, .T. ) ;
#4256=DIRECTION ( 'NONE',  ( -0.000000000000000000, -0.000000000000000000, 1.000000000000000000 ) ) ;
#4275=MECHANICAL_DESIGN_GEOMETRIC_PRESENTATION_REPRESENTATION('',(#7743),#5558);
#4299=AXIS2_PLACEMENT_3D ( 'NONE', #4858, #4256, #6540 ) ;
#4308=PLANE ( 'NONE',  #4969 ) ;
#4319=LINE ( 'NONE', #6176, #6339 ) ;
#4346=FACE_OUTER_BOUND ( 'NONE', #7306, .T. ) ;
#4374=ORIENTED_EDGE ( 'NONE', *, *, #395, .T. ) ;
#4381=DIRECTION ( 'NONE',  ( 1.000000000000000000, 0.000000000000000000, 0.000000000000000000 ) ) ;
#4439=FACE_OUTER_BOUND ( 'NONE', #4463, .T. ) ;
#4463=EDGE_LOOP ( 'NONE', ( #7415, #469, #4226, #4374 ) ) ;
#4480=DIRECTION ( 'NONE',  ( -0.000000000000000000, -0.000000000000000000, -1.000000000000000000 ) ) ;
#4486=( LENGTH_UNIT ( ) NAMED_UNIT ( * ) SI_UNIT ( .MILLI., .METRE. ) );
#4588=AXIS2_PLACEMENT_3D ( 'NONE', #793, #5508, #6899 ) ;
#4591=EDGE_LOOP ( 'NONE', ( #1351, #2929 ) ) ;
#4641=( NAMED_UNIT ( * ) SI_UNIT ( $, .STERADIAN. ) SOLID_ANGLE_UNIT ( ) );
#4675=AXIS2_PLACEMENT_3D ( 'NONE', #6536, #3004, #1035 ) ;
#4681=AXIS2_PLACEMENT_3D ( 'NONE', #5032, #1989, #1914 ) ;
#4685=ADVANCED_FACE ( 'NONE', ( #6463 ), #6504, .T. ) ;
#4719=CONICAL_SURFACE ( 'NONE', #4588, 12.50000000000000000, 0.7853981633974491672 ) ;
#4729=VERTEX_POINT ( 'NONE', #5825 ) ;
#4741=ORIENTED_EDGE ( 'NONE', *, *, #231, .F. ) ;
#4748=ORIENTED_EDGE ( 'NONE', *, *, #3565, .F. ) ;
#4767=CARTESIAN_POINT ( 'NONE',  ( 0.000000000000000000, 0.000000000000000000, 75.00000000000000000 ) ) ;
#4772=EDGE_CURVE ( 'NONE', #4729, #1108, #3808, .T. ) ;
#4774=SHAPE_DEFINITION_REPRESENTATION ( #275, #341 ) ;
#4787=DIRECTION ( 'NONE',  ( 1.000000000000000000, 0.000000000000000000, 0.000000000000000000 ) ) ;
#4849=AXIS2_PLACEMENT_3D ( 'NONE', #4767, #3661, #7311 ) ;
#4855=DIRECTION ( 'NONE',  ( 0.7071067811865482389, 0.000000000000000000, 0.7071067811865469066 ) ) ;
#4858=CARTESIAN_POINT ( 'NONE',  ( 0.000000000000000000, 0.000000000000000000, 2.000000000000001776 ) ) ;
#4874=ORIENTED_EDGE ( 'NONE', *, *, #3760, .T. ) ;
#4883=EDGE_CURVE ( 'NONE', #6898, #116, #1629, .T. ) ;
#4889=DIRECTION ( 'NONE',  ( 0.000000000000000000, -1.000000000000000000, 0.000000000000000000 ) ) ;
#4893=APPLICATION_CONTEXT ( 'automotive_design' ) ;
#4960=ORIENTED_EDGE ( 'NONE', *, *, #3760, .F. ) ;
#4969=AXIS2_PLACEMENT_3D ( 'NONE', #3085, #1269, #3117 ) ;
#5032=CARTESIAN_POINT ( 'NONE',  ( -12.50000000000000355, 1.530808498934191916E-15, 77.49999999999998579 ) ) ;
#5098=TOROIDAL_SURFACE ( 'NONE', #1647, 12.50000000000000355, 5.000000000000000000 ) ;
#5113=CARTESIAN_POINT ( 'NONE',  ( -12.50000000000000355, 1.836970198721030378E-15, 82.49999999999998579 ) ) ;
#5115=DIRECTION ( 'NONE',  ( 0.000000000000000000, 0.000000000000000000, 1.000000000000000000 ) ) ;
#5249=CARTESIAN_POINT ( 'NONE',  ( -12.50000000000000000, 0.000000000000000000, 2.000000000000001776 ) ) ;
#5293=EDGE_CURVE ( 'NONE', #1677, #2843, #5358, .T. ) ;
#5294=DIRECTION ( 'NONE',  ( 1.000000000000000000, 0.000000000000000000, 0.000000000000000000 ) ) ;
#5309=VECTOR ( 'NONE', #6932, 1000.000000000000000 ) ;
#5310=AXIS2_PLACEMENT_3D ( 'NONE', #6683, #1002, #3457 ) ;
#5358=CIRCLE ( 'NONE', #1004, 17.50000000000000355 ) ;
#5429=ADVANCED_FACE ( 'NONE', ( #4346 ), #4308, .F. ) ;
#5470=DIRECTION ( 'NONE',  ( -0.000000000000000000, -0.000000000000000000, 1.000000000000000000 ) ) ;
#5477=( NAMED_UNIT ( * ) SI_UNIT ( $, .STERADIAN. ) SOLID_ANGLE_UNIT ( ) );
#5502=DIRECTION ( 'NONE',  ( 1.000000000000000000, 0.000000000000000000, 0.000000000000000000 ) ) ;
#5508=DIRECTION ( 'NONE',  ( -0.000000000000000000, -0.000000000000000000, 1.000000000000000000 ) ) ;
#5558=( GEOMETRIC_REPRESENTATION_CONTEXT ( 3 ) GLOBAL_UNCERTAINTY_ASSIGNED_CONTEXT ( ( #6807 ) ) GLOBAL_UNIT_ASSIGNED_CONTEXT ( ( #4486, #7699, #4641 ) ) REPRESENTATION_CONTEXT ( 'NONE', 'WORKASPACE' ) );
#5574=AXIS2_PLACEMENT_3D ( 'NONE', #1180, #3078, #2315 ) ;
#5585=DIRECTION ( 'NONE',  ( 0.000000000000000000, 0.000000000000000000, -1.000000000000000000 ) ) ;
#5610=ORIENTED_EDGE ( 'NONE', *, *, #1254, .T. ) ;
#5634=DIRECTION ( 'NONE',  ( 1.000000000000000000, 0.000000000000000000, 0.000000000000000000 ) ) ;
#5662=ORIENTED_EDGE ( 'NONE', *, *, #4883, .T. ) ;
#5733=DIRECTION ( 'NONE',  ( -1.000000000000000000, 0.000000000000000000, 0.000000000000000000 ) ) ;
#5772=CARTESIAN_POINT ( 'NONE',  ( 0.000000000000000000, 0.000000000000000000, 77.49999999999998579 ) ) ;
#5785=AXIS2_PLACEMENT_3D ( 'NONE', #4110, #4186, #2351 ) ;
#5800=DIRECTION ( 'NONE',  ( -1.000000000000000000, 0.000000000000000000, 0.000000000000000000 ) ) ;
#5825=CARTESIAN_POINT ( 'NONE',  ( -10.49999999999999467, 1.408343819019455979E-15, 0.000000000000000000 ) ) ;
#5853=ORIENTED_EDGE ( 'NONE', *, *, #5936, .F. ) ;
#5856=DIRECTION ( 'NONE',  ( 0.000000000000000000, 0.000000000000000000, 1.000000000000000000 ) ) ;
#5917=EDGE_CURVE ( 'NONE', #6728, #3864, #6522, .T. ) ;
#5936=EDGE_CURVE ( 'NONE', #3881, #6488, #628, .T. ) ;
#5951=PRODUCT_CONTEXT ( 'NONE', #4893, 'mechanical' ) ;
#5959=TOROIDAL_SURFACE ( 'NONE', #3651, 12.50000000000000355, 5.000000000000000000 ) ;
#5965=EDGE_LOOP ( 'NONE', ( #5662, #7767 ) ) ;
#5986=AXIS2_PLACEMENT_3D ( 'NONE', #6509, #1486, #2736 ) ;
#6034=DIRECTION ( 'NONE',  ( -1.000000000000000000, 0.000000000000000000, 0.000000000000000000 ) ) ;
#6069=CYLINDRICAL_SURFACE ( 'NONE', #3953, 17.50000000000000355 ) ;
#6100=ORIENTED_EDGE ( 'NONE', *, *, #2937, .T. ) ;
#6154=CARTESIAN_POINT ( 'NONE',  ( 0.000000000000000000, 0.000000000000000000, 82.49999999999998579 ) ) ;
#6176=CARTESIAN_POINT ( 'NONE',  ( -12.50000000000000000, 1.530808498934191521E-15, 2.000000000000001776 ) ) ;
#6206=VECTOR ( 'NONE', #844, 1000.000000000000000 ) ;
#6230=CARTESIAN_POINT ( 'NONE',  ( 0.000000000000000000, 0.000000000000000000, 82.49999999999998579 ) ) ;
#6241=AXIS2_PLACEMENT_3D ( 'NONE', #3618, #2861, #5294 ) ;
#6279=CARTESIAN_POINT ( 'NONE',  ( 0.000000000000000000, 0.000000000000000000, 82.49999999999998579 ) ) ;
#6303=ADVANCED_FACE ( 'NONE', ( #7827, #7791 ), #2336, .F. ) ;
#6328=EDGE_CURVE ( 'NONE', #1785, #6488, #1016, .T. ) ;
#6339=VECTOR ( 'NONE', #3170, 999.9999999999998863 ) ;
#6340=CARTESIAN_POINT ( 'NONE',  ( -17.50000000000000355, 0.000000000000000000, 82.49999999999998579 ) ) ;
#6368=LINE ( 'NONE', #305, #833 ) ;
#6371=CARTESIAN_POINT ( 'NONE',  ( 0.000000000000000000, 0.000000000000000000, 0.000000000000000000 ) ) ;
#6378=LINE ( 'NONE', #6340, #6206 ) ;
#6414=ORIENTED_EDGE ( 'NONE', *, *, #2959, .T. ) ;
#6416=ORIENTED_EDGE ( 'NONE', *, *, #5917, .T. ) ;
#6433=DIRECTION ( 'NONE',  ( -0.000000000000000000, -0.000000000000000000, -1.000000000000000000 ) ) ;
#6443=DIRECTION ( 'NONE',  ( -0.000000000000000000, -0.000000000000000000, -1.000000000000000000 ) ) ;
#6463=FACE_OUTER_BOUND ( 'NONE', #93, .T. ) ;
#6488=VERTEX_POINT ( 'NONE', #2003 ) ;
#6504=CONICAL_SURFACE ( 'NONE', #5986, 12.50000000000000000, 0.7853981633974491672 ) ;
#6509=CARTESIAN_POINT ( 'NONE',  ( 0.000000000000000000, 0.000000000000000000, 2.000000000000001776 ) ) ;
#6522=CIRCLE ( 'NONE', #366, 12.50000000000000000 ) ;
#6536=CARTESIAN_POINT ( 'NONE',  ( 0.000000000000000000, 0.000000000000000000, 82.49999999999998579 ) ) ;
#6540=DIRECTION ( 'NONE',  ( 1.000000000000000000, 0.000000000000000000, 0.000000000000000000 ) ) ;
#6550=CARTESIAN_POINT ( 'NONE',  ( 0.000000000000000000, 0.000000000000000000, 77.49999999999998579 ) ) ;
#6564=ORIENTED_EDGE ( 'NONE', *, *, #1448, .T. ) ;
#6579=CLOSED_SHELL ( 'NONE', ( #4685, #1622, #3211, #3029, #1734, #5429, #7346, #633, #6303, #6869, #7341 ) ) ;
#6580=ORIENTED_EDGE ( 'NONE', *, *, #5293, .T. ) ;
#6636=CARTESIAN_POINT ( 'NONE',  ( 17.50000000000000355, 2.143131898507868643E-15, 77.49999999999998579 ) ) ;
#6683=CARTESIAN_POINT ( 'NONE',  ( 0.000000000000000000, 0.000000000000000000, 77.49999999999998579 ) ) ;
#6697=ORIENTED_EDGE ( 'NONE', *, *, #2265, .F. ) ;
#6709=CARTESIAN_POINT ( 'NONE',  ( 0.000000000000000000, 0.000000000000000000, 2.000000000000001776 ) ) ;
#6728=VERTEX_POINT ( 'NONE', #5249 ) ;
#6807=UNCERTAINTY_MEASURE_WITH_UNIT (LENGTH_MEASURE( 1.000000000000000082E-05 ), #4486, 'distance_accuracy_value', 'NONE');
#6869=ADVANCED_FACE ( 'NONE', ( #3169 ), #5098, .T. ) ;
#6885=PRODUCT_DEFINITION ( 'UNKNOWN', '', #3106, #3985 ) ;
#6898=VERTEX_POINT ( 'NONE', #753 ) ;
#6899=DIRECTION ( 'NONE',  ( 1.000000000000000000, 0.000000000000000000, 0.000000000000000000 ) ) ;
#6932=DIRECTION ( 'NONE',  ( -0.000000000000000000, -0.000000000000000000, -1.000000000000000000 ) ) ;
#6955=ORIENTED_EDGE ( 'NONE', *, *, #473, .T. ) ;
#7122=DIRECTION ( 'NONE',  ( -0.000000000000000000, -0.000000000000000000, -1.000000000000000000 ) ) ;
#7306=EDGE_LOOP ( 'NONE', ( #7422, #2467 ) ) ;
#7311=DIRECTION ( 'NONE',  ( 1.000000000000000000, 0.000000000000000000, -0.000000000000000000 ) ) ;
#7312=CARTESIAN_POINT ( 'NONE',  ( 12.50000000000000000, 0.000000000000000000, 2.000000000000001776 ) ) ;
#7341=ADVANCED_FACE ( 'NONE', ( #7498 ), #4719, .T. ) ;
#7346=ADVANCED_FACE ( 'NONE', ( #4439 ), #6069, .T. ) ;
#7358=DIRECTION ( 'NONE',  ( 1.000000000000000000, 0.000000000000000000, -0.000000000000000000 ) ) ;
#7366=AXIS2_PLACEMENT_3D ( 'NONE', #3282, #351, #5733 ) ;
#7368=CIRCLE ( 'NONE', #5310, 17.50000000000000355 ) ;
#7415=ORIENTED_EDGE ( 'NONE', *, *, #2959, .F. ) ;
#7421=CARTESIAN_POINT ( 'NONE',  ( -17.50000000000000355, 0.000000000000000000, 75.00000000000000000 ) ) ;
#7422=ORIENTED_EDGE ( 'NONE', *, *, #7458, .T. ) ;
#7458=EDGE_CURVE ( 'NONE', #1108, #4729, #1135, .T. ) ;
#7498=FACE_OUTER_BOUND ( 'NONE', #931, .T. ) ;
#7635=CARTESIAN_POINT ( 'NONE',  ( 17.50000000000000355, 2.143131898507868643E-15, 75.00000000000000000 ) ) ;
#7650=ORIENTED_EDGE ( 'NONE', *, *, #2984, .T. ) ;
#7699=( NAMED_UNIT ( * ) PLANE_ANGLE_UNIT ( ) SI_UNIT ( $, .RADIAN. ) );
#7720=ORIENTED_EDGE ( 'NONE', *, *, #6328, .T. ) ;
#7743=STYLED_ITEM('',(#7969),#1383);
#7750=AXIS2_PLACEMENT_3D ( 'NONE', #6154, #2540, #7358 ) ;
#7767=ORIENTED_EDGE ( 'NONE', *, *, #1831, .T. ) ;
#7791=FACE_OUTER_BOUND ( 'NONE', #4591, .T. ) ;
#7792=CARTESIAN_POINT ( 'NONE',  ( 10.49999999999999467, 0.000000000000000000, 0.000000000000000000 ) ) ;
#7820=APPLICATION_CONTEXT ( 'automotive_design' ) ;
#7827=FACE_BOUND ( 'NONE', #5965, .T. ) ;
#7877=EDGE_LOOP ( 'NONE', ( #1152, #3082, #7650, #6416 ) ) ;
#7881=ORIENTED_EDGE ( 'NONE', *, *, #5936, .T. ) ;
#7963=COLOUR_RGB('Black',0.12,0.14,0.17);
#7964=FILL_AREA_STYLE_COLOUR('',#7963);
#7965=FILL_AREA_STYLE('',(#7964));
#7966=SURFACE_STYLE_FILL_AREA(#7965);
#7967=SURFACE_SIDE_STYLE('',(#7966));
#7968=SURFACE_STYLE_USAGE(.BOTH.,#7967);
#7969=PRESENTATION_STYLE_ASSIGNMENT((#7968));
ENDSEC;
END-ISO-10303-21;
